ISO-10303-21;
HEADER;
/* Generated by software containing ST-Developer
 * from STEP Tools, Inc. (www.steptools.com) 
 */

FILE_DESCRIPTION(
/* description */ ('PAT-072'),
/* implementation_level */ '2;1');

FILE_NAME(
/* name */ 'Metering plug.step',
/* time_stamp */ '2026-10-29T20:11:56-07:00',
/* author */ (''),
/* organization */ (''),
/* preprocessor_version */ 'ST-DEVELOPER v20.2',
/* originating_system */ 'Autodesk Translation Framework v15.17.0.0',
/* authorisation */ '');

FILE_SCHEMA (('AUTOMOTIVE_DESIGN { 1 0 10303 214 3 1 1 }'));
ENDSEC;

DATA;
#10=MECHANICAL_DESIGN_GEOMETRIC_PRESENTATION_REPRESENTATION('',(#337),#11432);
#265=SHAPE_REPRESENTATION_RELATIONSHIP('SRR','None',#11569,#301);
#301=ADVANCED_BREP_SHAPE_REPRESENTATION('',(#373),#11400);
#337=STYLED_ITEM('',(#11812),#373);
#373=MANIFOLD_SOLID_BREP('Body1',#6072);
#462=FACE_BOUND('',#1330,.T.);
#463=FACE_BOUND('',#1334,.T.);
#623=PLANE('',#6702);
#624=PLANE('',#6707);
#625=PLANE('',#6708);
#626=PLANE('',#6714);
#897=FACE_OUTER_BOUND('',#1329,.T.);
#898=FACE_OUTER_BOUND('',#1331,.T.);
#899=FACE_OUTER_BOUND('',#1332,.T.);
#900=FACE_OUTER_BOUND('',#1333,.T.);
#901=FACE_OUTER_BOUND('',#1335,.T.);
#902=FACE_OUTER_BOUND('',#1336,.T.);
#903=FACE_OUTER_BOUND('',#1337,.T.);
#1329=EDGE_LOOP('',(#4510));
#1330=EDGE_LOOP('',(#4511));
#1331=EDGE_LOOP('',(#4512,#4513,#4514,#4515));
#1332=EDGE_LOOP('',(#4516));
#1333=EDGE_LOOP('',(#4517));
#1334=EDGE_LOOP('',(#4518));
#1335=EDGE_LOOP('',(#4519,#4520,#4521,#4522));
#1336=EDGE_LOOP('',(#4523,#4524,#4525,#4526));
#1337=EDGE_LOOP('',(#4527));
#1812=LINE('',#10012,#2231);
#1813=LINE('',#10020,#2232);
#1814=LINE('',#10023,#2233);
#2231=VECTOR('',#7773,0.6);
#2232=VECTOR('',#7784,0.3);
#2233=VECTOR('',#7787,0.1);
#2631=CIRCLE('',#6703,0.6);
#2632=CIRCLE('',#6704,0.3);
#2633=CIRCLE('',#6706,0.6);
#2634=CIRCLE('',#6709,0.3);
#2635=CIRCLE('',#6710,0.1);
#2636=CIRCLE('',#6713,0.1);
#2980=VERTEX_POINT('',#10005);
#2981=VERTEX_POINT('',#10007);
#2982=VERTEX_POINT('',#10010);
#2983=VERTEX_POINT('',#10015);
#2984=VERTEX_POINT('',#10017);
#2985=VERTEX_POINT('',#10022);
#3544=EDGE_CURVE('',#2980,#2980,#2631,.T.);
#3545=EDGE_CURVE('',#2981,#2981,#2632,.T.);
#3546=EDGE_CURVE('',#2982,#2982,#2633,.T.);
#3547=EDGE_CURVE('',#2982,#2980,#1812,.T.);
#3548=EDGE_CURVE('',#2983,#2983,#2634,.T.);
#3549=EDGE_CURVE('',#2984,#2984,#2635,.T.);
#3550=EDGE_CURVE('',#2981,#2983,#1813,.T.);
#3551=EDGE_CURVE('',#2984,#2985,#1814,.T.);
#3552=EDGE_CURVE('',#2985,#2985,#2636,.T.);
#4510=ORIENTED_EDGE('',*,*,#3544,.F.);
#4511=ORIENTED_EDGE('',*,*,#3545,.T.);
#4512=ORIENTED_EDGE('',*,*,#3546,.F.);
#4513=ORIENTED_EDGE('',*,*,#3547,.T.);
#4514=ORIENTED_EDGE('',*,*,#3544,.T.);
#4515=ORIENTED_EDGE('',*,*,#3547,.F.);
#4516=ORIENTED_EDGE('',*,*,#3546,.T.);
#4517=ORIENTED_EDGE('',*,*,#3548,.F.);
#4518=ORIENTED_EDGE('',*,*,#3549,.T.);
#4519=ORIENTED_EDGE('',*,*,#3545,.F.);
#4520=ORIENTED_EDGE('',*,*,#3550,.T.);
#4521=ORIENTED_EDGE('',*,*,#3548,.T.);
#4522=ORIENTED_EDGE('',*,*,#3550,.F.);
#4523=ORIENTED_EDGE('',*,*,#3549,.F.);
#4524=ORIENTED_EDGE('',*,*,#3551,.T.);
#4525=ORIENTED_EDGE('',*,*,#3552,.T.);
#4526=ORIENTED_EDGE('',*,*,#3551,.F.);
#4527=ORIENTED_EDGE('',*,*,#3552,.F.);
#5606=CYLINDRICAL_SURFACE('',#6705,0.6);
#5607=CYLINDRICAL_SURFACE('',#6711,0.3);
#5608=CYLINDRICAL_SURFACE('',#6712,0.1);
#5796=ADVANCED_FACE('',(#897,#462),#623,.F.);
#5797=ADVANCED_FACE('',(#898),#5606,.T.);
#5798=ADVANCED_FACE('',(#899),#624,.T.);
#5799=ADVANCED_FACE('',(#900,#463),#625,.F.);
#5800=ADVANCED_FACE('',(#901),#5607,.T.);
#5801=ADVANCED_FACE('',(#902),#5608,.T.);
#5802=ADVANCED_FACE('',(#903),#626,.F.);
#6072=CLOSED_SHELL('',(#5796,#5797,#5798,#5799,#5800,#5801,#5802));
#6701=AXIS2_PLACEMENT_3D('',#10003,#7761,#7762);
#6702=AXIS2_PLACEMENT_3D('',#10004,#7763,#7764);
#6703=AXIS2_PLACEMENT_3D('',#10006,#7765,#7766);
#6704=AXIS2_PLACEMENT_3D('',#10008,#7767,#7768);
#6705=AXIS2_PLACEMENT_3D('',#10009,#7769,#7770);
#6706=AXIS2_PLACEMENT_3D('',#10011,#7771,#7772);
#6707=AXIS2_PLACEMENT_3D('',#10013,#7774,#7775);
#6708=AXIS2_PLACEMENT_3D('',#10014,#7776,#7777);
#6709=AXIS2_PLACEMENT_3D('',#10016,#7778,#7779);
#6710=AXIS2_PLACEMENT_3D('',#10018,#7780,#7781);
#6711=AXIS2_PLACEMENT_3D('',#10019,#7782,#7783);
#6712=AXIS2_PLACEMENT_3D('',#10021,#7785,#7786);
#6713=AXIS2_PLACEMENT_3D('',#10024,#7788,#7789);
#6714=AXIS2_PLACEMENT_3D('',#10025,#7790,#7791);
#7761=DIRECTION('axis',(0.,0.,1.));
#7762=DIRECTION('refdir',(1.,0.,0.));
#7763=DIRECTION('center_axis',(0.,0.,1.));
#7764=DIRECTION('ref_axis',(1.,0.,0.));
#7765=DIRECTION('center_axis',(0.,0.,1.));
#7766=DIRECTION('ref_axis',(1.,0.,0.));
#7767=DIRECTION('center_axis',(0.,0.,1.));
#7768=DIRECTION('ref_axis',(1.,0.,0.));
#7769=DIRECTION('center_axis',(0.,0.,1.));
#7770=DIRECTION('ref_axis',(1.,0.,0.));
#7771=DIRECTION('center_axis',(0.,0.,1.));
#7772=DIRECTION('ref_axis',(1.,0.,0.));
#7773=DIRECTION('',(0.,0.,-1.));
#7774=DIRECTION('center_axis',(0.,0.,1.));
#7775=DIRECTION('ref_axis',(1.,0.,0.));
#7776=DIRECTION('center_axis',(0.,0.,1.));
#7777=DIRECTION('ref_axis',(1.,0.,0.));
#7778=DIRECTION('center_axis',(0.,0.,1.));
#7779=DIRECTION('ref_axis',(1.,0.,0.));
#7780=DIRECTION('center_axis',(0.,0.,1.));
#7781=DIRECTION('ref_axis',(1.,0.,0.));
#7782=DIRECTION('center_axis',(0.,0.,1.));
#7783=DIRECTION('ref_axis',(1.,0.,0.));
#7784=DIRECTION('',(0.,0.,-1.));
#7785=DIRECTION('center_axis',(0.,0.,1.));
#7786=DIRECTION('ref_axis',(1.,0.,0.));
#7787=DIRECTION('',(0.,0.,-1.));
#7788=DIRECTION('center_axis',(0.,0.,1.));
#7789=DIRECTION('ref_axis',(1.,0.,0.));
#7790=DIRECTION('center_axis',(0.,0.,1.));
#7791=DIRECTION('ref_axis',(1.,0.,0.));
#10003=CARTESIAN_POINT('',(0.,0.,0.));
#10004=CARTESIAN_POINT('Origin',(-3.75,1.5,6.1));
#10005=CARTESIAN_POINT('',(-4.35,1.5,6.1));
#10006=CARTESIAN_POINT('Origin',(-3.75,1.5,6.1));
#10007=CARTESIAN_POINT('',(-4.05,1.5,6.1));
#10008=CARTESIAN_POINT('Origin',(-3.75,1.5,6.1));
#10009=CARTESIAN_POINT('Origin',(-3.75,1.5,6.1));
#10010=CARTESIAN_POINT('',(-4.35,1.5,6.5));
#10011=CARTESIAN_POINT('Origin',(-3.75,1.5,6.5));
#10012=CARTESIAN_POINT('',(-4.35,1.5,6.1));
#10013=CARTESIAN_POINT('Origin',(-3.75,1.5,6.5));
#10014=CARTESIAN_POINT('Origin',(-3.75,1.5,4.8));
#10015=CARTESIAN_POINT('',(-4.05,1.5,4.8));
#10016=CARTESIAN_POINT('Origin',(-3.75,1.5,4.8));
#10017=CARTESIAN_POINT('',(-3.85,1.5,4.8));
#10018=CARTESIAN_POINT('Origin',(-3.75,1.5,4.8));
#10019=CARTESIAN_POINT('Origin',(-3.75,1.5,4.8));
#10020=CARTESIAN_POINT('',(-4.05,1.5,4.8));
#10021=CARTESIAN_POINT('Origin',(-3.75,1.5,4.1));
#10022=CARTESIAN_POINT('',(-3.85,1.5,4.1));
#10023=CARTESIAN_POINT('',(-3.85,1.5,4.1));
#10024=CARTESIAN_POINT('Origin',(-3.75,1.5,4.1));
#10025=CARTESIAN_POINT('Origin',(-3.75,1.5,4.1));
#11361=UNCERTAINTY_MEASURE_WITH_UNIT(LENGTH_MEASURE(0.001),#11433,
'DISTANCE_ACCURACY_VALUE',
'Maximum model space distance between geometric entities at asserted c
onnectivities');
#11393=UNCERTAINTY_MEASURE_WITH_UNIT(LENGTH_MEASURE(0.001),#11433,
'DISTANCE_ACCURACY_VALUE',
'Maximum model space distance between geometric entities at asserted c
onnectivities');
#11400=(
GEOMETRIC_REPRESENTATION_CONTEXT(3)
GLOBAL_UNCERTAINTY_ASSIGNED_CONTEXT((#11361))
GLOBAL_UNIT_ASSIGNED_CONTEXT((#11433,#11435,#11436))
REPRESENTATION_CONTEXT('','3D')
);
#11432=(
GEOMETRIC_REPRESENTATION_CONTEXT(3)
GLOBAL_UNCERTAINTY_ASSIGNED_CONTEXT((#11393))
GLOBAL_UNIT_ASSIGNED_CONTEXT((#11433,#11435,#11436))
REPRESENTATION_CONTEXT('','3D')
);
#11433=(
LENGTH_UNIT()
NAMED_UNIT(*)
SI_UNIT(.CENTI.,.METRE.)
);
#11435=(
NAMED_UNIT(*)
PLANE_ANGLE_UNIT()
SI_UNIT($,.RADIAN.)
);
#11436=(
NAMED_UNIT(*)
SI_UNIT($,.STERADIAN.)
SOLID_ANGLE_UNIT()
);
#11443=SHAPE_DEFINITION_REPRESENTATION(#11481,#11569);
#11481=PRODUCT_DEFINITION_SHAPE('',$,#11608);
#11569=SHAPE_REPRESENTATION('',(#6701),#11400);
#11601=PRODUCT_DEFINITION_CONTEXT('part definition',#11717,'design');
#11608=PRODUCT_DEFINITION('Metering plug','Metering plug',#11646,
#11601);
#11646=PRODUCT_DEFINITION_FORMATION('',$,#11725);
#11717=APPLICATION_CONTEXT(
'Core Data for Automotive Mechanical Design Process');
#11718=PRODUCT_CONTEXT('part definition',#11717,'mechanical');
#11725=PRODUCT('Metering plug','Metering plug',
'Metering plug',(#11718));
#11806=COLOUR_RGB('Sky Blue',0.24,0.69,0.87);
#11807=FILL_AREA_STYLE_COLOUR('',#11806);
#11808=FILL_AREA_STYLE('',(#11807));
#11809=SURFACE_STYLE_FILL_AREA(#11808);
#11810=SURFACE_SIDE_STYLE('',(#11809));
#11811=SURFACE_STYLE_USAGE(.BOTH.,#11810);
#11812=PRESENTATION_STYLE_ASSIGNMENT((#11811));
ENDSEC;
END-ISO-10303-21;
